ISO-10303-21;
HEADER;
FILE_DESCRIPTION (('STEP AP214'),
    '1' );
FILE_NAME ('circlip for shafts normal_din_Circlip DIN 471 - 10 x 1.step',
    '2026-10-31T03:44:21',
    ( '' ),
    ( '' ),
    'SwSTEP 2.0',
    'SolidWorks 2026',
    '' );
FILE_SCHEMA (( 'AUTOMOTIVE_DESIGN' ));
ENDSEC;

DATA;
#40=VERTEX_POINT ( 'NONE', #10112 ) ;
#139=CARTESIAN_POINT ( 'NONE',  ( -0.2500000000000000000, -8.096141056083446585, -1.000000000000000000 ) ) ;
#157=ORIENTED_EDGE ( 'NONE', *, *, #5820, .T. ) ;
#161=DIRECTION ( 'NONE',  ( 0.000000000000000000, 0.000000000000000000, 1.000000000000000000 ) ) ;
#234=DIRECTION ( 'NONE',  ( 0.000000000000000000, 0.000000000000000000, 1.000000000000000000 ) ) ;
#243=VECTOR ( 'NONE', #1548, 1000.000000000000114 ) ;
#253=DIRECTION ( 'NONE',  ( 1.000000000000000000, 0.000000000000000000, 0.000000000000000000 ) ) ;
#303=DIRECTION ( 'NONE',  ( 0.000000000000000000, 0.000000000000000000, 1.000000000000000000 ) ) ;
#307=ORIENTED_EDGE ( 'NONE', *, *, #12740, .F. ) ;
#369=ADVANCED_FACE ( 'NONE', ( #6760 ), #18743, .T. ) ;
#371=DIRECTION ( 'NONE',  ( 1.000000000000000000, 0.000000000000000000, 0.000000000000000000 ) ) ;
#417=EDGE_CURVE ( 'NONE', #1879, #10892, #2680, .T. ) ;
#432=DIRECTION ( 'NONE',  ( 0.000000000000000000, 0.000000000000000000, 1.000000000000000000 ) ) ;
#510=CARTESIAN_POINT ( 'NONE',  ( -0.2500000000000000000, -8.096141056083446585, 0.000000000000000000 ) ) ;
#525=EDGE_CURVE ( 'NONE', #728, #14377, #18969, .T. ) ;
#591=EDGE_CURVE ( 'NONE', #11915, #8974, #13845, .T. ) ;
#611=DIRECTION ( 'NONE',  ( 1.000000000000000000, 0.000000000000000000, 0.000000000000000000 ) ) ;
#615=LINE ( 'NONE', #12469, #11701 ) ;
#653=AXIS2_PLACEMENT_3D ( 'NONE', #11372, #801, #895 ) ;
#683=PRODUCT ( 'circlip for shafts normal_din_Circlip DIN 471 - 10 x 1', 'circlip for shafts normal_din_Circlip DIN 471 - 10 x 1', '', ( #1686 ) ) ;
#728=VERTEX_POINT ( 'NONE', #17418 ) ;
#773=EDGE_CURVE ( 'NONE', #14662, #8385, #13542, .T. ) ;
#786=ORIENTED_EDGE ( 'NONE', *, *, #16950, .T. ) ;
#801=DIRECTION ( 'NONE',  ( 0.9914448613738102711, -0.1305261922200524338, 0.000000000000000000 ) ) ;
#823=ORIENTED_EDGE ( 'NONE', *, *, #2475, .T. ) ;
#825=ORIENTED_EDGE ( 'NONE', *, *, #1368, .F. ) ;
#853=CARTESIAN_POINT ( 'NONE',  ( 0.000000000000000000, 0.000000000000000000, -1.000000000000000000 ) ) ;
#859=EDGE_LOOP ( 'NONE', ( #17158, #4161, #12348, #6970 ) ) ;
#873=DIRECTION ( 'NONE',  ( 0.000000000000000000, 0.000000000000000000, 1.000000000000000000 ) ) ;
#880=EDGE_CURVE ( 'NONE', #17434, #10530, #14790, .T. ) ;
#895=DIRECTION ( 'NONE',  ( 0.1305261922200524338, 0.9914448613738102711, 0.000000000000000000 ) ) ;
#912=DIRECTION ( 'NONE',  ( 0.000000000000000000, 0.000000000000000000, 1.000000000000000000 ) ) ;
#929=FACE_BOUND ( 'NONE', #9121, .T. ) ;
#944=VECTOR ( 'NONE', #12350, 999.9999999999998863 ) ;
#983=VERTEX_POINT ( 'NONE', #10427 ) ;
#1007=CIRCLE ( 'NONE', #7575, 0.7499999999999997780 ) ;
#1071=ORIENTED_EDGE ( 'NONE', *, *, #3385, .F. ) ;
#1075=DIRECTION ( 'NONE',  ( 1.000000000000000000, 0.000000000000000000, 0.000000000000000000 ) ) ;
#1082=LINE ( 'NONE', #16085, #10346 ) ;
#1106=EDGE_CURVE ( 'NONE', #13173, #8267, #17198, .T. ) ;
#1124=ORIENTED_EDGE ( 'NONE', *, *, #11802, .T. ) ;
#1126=VERTEX_POINT ( 'NONE', #13937 ) ;
#1175=ADVANCED_FACE ( 'NONE', ( #1910 ), #12378, .F. ) ;
#1215=CARTESIAN_POINT ( 'NONE',  ( 3.309651814758564736, -5.455921364805393026, 0.000000000000000000 ) ) ;
#1256=EDGE_CURVE ( 'NONE', #4089, #983, #12142, .T. ) ;
#1284=AXIS2_PLACEMENT_3D ( 'NONE', #12742, #14108, #3631 ) ;
#1305=DIRECTION ( 'NONE',  ( 0.1305261922200524616, 0.9914448613738103822, -0.000000000000000000 ) ) ;
#1319=ORIENTED_EDGE ( 'NONE', *, *, #16055, .T. ) ;
#1348=ORIENTED_EDGE ( 'NONE', *, *, #12740, .T. ) ;
#1368=EDGE_CURVE ( 'NONE', #3316, #16919, #2782, .T. ) ;
#1371=DIRECTION ( 'NONE',  ( 0.000000000000000000, 0.000000000000000000, 1.000000000000000000 ) ) ;
#1394=APPLICATION_CONTEXT ( 'automotive_design' ) ;
#1478=AXIS2_PLACEMENT_3D ( 'NONE', #7872, #4839, #2090 ) ;
#1548=DIRECTION ( 'NONE',  ( 0.03086419753086420623, -0.9995235871707959241, 0.000000000000000000 ) ) ;
#1632=AXIS2_PLACEMENT_3D ( 'NONE', #16940, #17303, #18232 ) ;
#1645=CARTESIAN_POINT ( 'NONE',  ( 0.000000000000000000, 0.5192545390863916310, -1.000000000000000000 ) ) ;
#1647=ORIENTED_EDGE ( 'NONE', *, *, #11926, .F. ) ;
#1669=ORIENTED_EDGE ( 'NONE', *, *, #7372, .T. ) ;
#1686=PRODUCT_CONTEXT ( 'NONE', #1394, 'mechanical' ) ;
#1711=DIRECTION ( 'NONE',  ( 0.000000000000000000, 0.000000000000000000, 1.000000000000000000 ) ) ;
#1718=LINE ( 'NONE', #5130, #3483 ) ;
#1741=ADVANCED_FACE ( 'NONE', ( #1887 ), #7759, .T. ) ;
#1755=ORIENTED_EDGE ( 'NONE', *, *, #4727, .T. ) ;
#1776=SHAPE_DEFINITION_REPRESENTATION ( #8187, #11935 ) ;
#1800=EDGE_CURVE ( 'NONE', #15771, #11016, #9606, .T. ) ;
#1811=( NAMED_UNIT ( * ) PLANE_ANGLE_UNIT ( ) SI_UNIT ( $, .RADIAN. ) );
#1879=VERTEX_POINT ( 'NONE', #10385 ) ;
#1887=FACE_OUTER_BOUND ( 'NONE', #7540, .T. ) ;
#1892=VECTOR ( 'NONE', #8776, 1000.000000000000000 ) ;
#1910=FACE_OUTER_BOUND ( 'NONE', #18333, .T. ) ;
#1951=ORIENTED_EDGE ( 'NONE', *, *, #17793, .F. ) ;
#2044=ORIENTED_EDGE ( 'NONE', *, *, #12883, .F. ) ;
#2090=DIRECTION ( 'NONE',  ( 1.000000000000000000, 0.000000000000000000, 0.000000000000000000 ) ) ;
#2130=VERTEX_POINT ( 'NONE', #6451 ) ;
#2140=ORIENTED_EDGE ( 'NONE', *, *, #5820, .F. ) ;
#2146=ORIENTED_EDGE ( 'NONE', *, *, #16593, .T. ) ;
#2158=ORIENTED_EDGE ( 'NONE', *, *, #1256, .F. ) ;
#2211=CIRCLE ( 'NONE', #10026, 8.099999999999999645 ) ;
#2226=CARTESIAN_POINT ( 'NONE',  ( 5.686050877451574337, -5.768780236673276995, -1.000000000000000000 ) ) ;
#2249=DIRECTION ( 'NONE',  ( 0.000000000000000000, 0.000000000000000000, 1.000000000000000000 ) ) ;
#2251=MECHANICAL_DESIGN_GEOMETRIC_PRESENTATION_REPRESENTATION('',(#17791),#19282);
#2271=ADVANCED_FACE ( 'NONE', ( #10165, #17256, #3027 ), #5965, .F. ) ;
#2274=EDGE_CURVE ( 'NONE', #5177, #8267, #5504, .T. ) ;
#2279=DIRECTION ( 'NONE',  ( 0.000000000000000000, 0.000000000000000000, 1.000000000000000000 ) ) ;
#2301=PRODUCT_DEFINITION_FORMATION_WITH_SPECIFIED_SOURCE ( 'ANY', '', #683, .NOT_KNOWN. ) ;
#2344=ORIENTED_EDGE ( 'NONE', *, *, #880, .T. ) ;
#2388=EDGE_CURVE ( 'NONE', #16919, #15771, #16974, .T. ) ;
#2419=FACE_OUTER_BOUND ( 'NONE', #859, .T. ) ;
#2429=CIRCLE ( 'NONE', #1478, 0.7500000000000000000 ) ;
#2434=EDGE_LOOP ( 'NONE', ( #5923, #823, #6971, #7270 ) ) ;
#2475=EDGE_CURVE ( 'NONE', #2828, #10144, #6623, .T. ) ;
#2564=( LENGTH_UNIT ( ) NAMED_UNIT ( * ) SI_UNIT ( .MILLI., .METRE. ) );
#2571=ORIENTED_EDGE ( 'NONE', *, *, #16055, .F. ) ;
#2582=DIRECTION ( 'NONE',  ( 1.000000000000000000, 0.000000000000000000, 0.000000000000000000 ) ) ;
#2641=ORIENTED_EDGE ( 'NONE', *, *, #5482, .F. ) ;
#2659=CARTESIAN_POINT ( 'NONE',  ( 4.078421086530217288, -3.990950201428958621, -1.000000000000000000 ) ) ;
#2680=CIRCLE ( 'NONE', #13918, 2.396904916527699214 ) ;
#2690=CYLINDRICAL_SURFACE ( 'NONE', #5451, 0.7500000000000000000 ) ;
#2704=ORIENTED_EDGE ( 'NONE', *, *, #2799, .F. ) ;
#2780=STYLED_ITEM ( 'NONE', ( #19131 ), #15256 ) ;
#2782=LINE ( 'NONE', #18772, #6479 ) ;
#2789=VECTOR ( 'NONE', #15781, 1000.000000000000000 ) ;
#2795=LINE ( 'NONE', #7482, #12483 ) ;
#2799=EDGE_CURVE ( 'NONE', #3316, #16533, #1007, .T. ) ;
#2828=VERTEX_POINT ( 'NONE', #3729 ) ;
#2871=CARTESIAN_POINT ( 'NONE',  ( 0.000000000000000000, 0.000000000000000000, 0.000000000000000000 ) ) ;
#2891=DIRECTION ( 'NONE',  ( 1.000000000000000000, 0.000000000000000000, 0.000000000000000000 ) ) ;
#2946=VERTEX_POINT ( 'NONE', #16451 ) ;
#2948=CYLINDRICAL_SURFACE ( 'NONE', #12723, 0.7500000000000000000 ) ;
#2965=ORIENTED_EDGE ( 'NONE', *, *, #10349, .F. ) ;
#2974=CYLINDRICAL_SURFACE ( 'NONE', #13266, 0.7500000000000000000 ) ;
#2980=CIRCLE ( 'NONE', #7969, 4.799999999999999822 ) ;
#3027=FACE_OUTER_BOUND ( 'NONE', #15849, .T. ) ;
#3048=DIRECTION ( 'NONE',  ( 0.03086419753086420623, 0.9995235871707959241, 0.000000000000000000 ) ) ;
#3089=ORIENTED_EDGE ( 'NONE', *, *, #18187, .T. ) ;
#3096=DIRECTION ( 'NONE',  ( 1.000000000000000000, 0.000000000000000000, 0.000000000000000000 ) ) ;
#3124=DIRECTION ( 'NONE',  ( 1.000000000000000000, 0.000000000000000000, 0.000000000000000000 ) ) ;
#3130=DIRECTION ( 'NONE',  ( 1.000000000000000000, 0.000000000000000000, 0.000000000000000000 ) ) ;
#3146=AXIS2_PLACEMENT_3D ( 'NONE', #8448, #6484, #611 ) ;
#3148=PLANE ( 'NONE',  #16136 ) ;
#3159=ADVANCED_FACE ( 'NONE', ( #3682 ), #9648, .F. ) ;
#3166=AXIS2_PLACEMENT_3D ( 'NONE', #17566, #1371, #12936 ) ;
#3206=VERTEX_POINT ( 'NONE', #10134 ) ;
#3249=DIRECTION ( 'NONE',  ( 0.000000000000000000, 0.000000000000000000, 1.000000000000000000 ) ) ;
#3250=ORIENTED_EDGE ( 'NONE', *, *, #10236, .F. ) ;
#3316=VERTEX_POINT ( 'NONE', #7586 ) ;
#3385=EDGE_CURVE ( 'NONE', #4604, #1126, #13262, .T. ) ;
#3450=VECTOR ( 'NONE', #6682, 1000.000000000000000 ) ;
#3459=CARTESIAN_POINT ( 'NONE',  ( 0.000000000000000000, 0.000000000000000000, -1.000000000000000000 ) ) ;
#3483=VECTOR ( 'NONE', #8357, 1000.000000000000000 ) ;
#3487=ORIENTED_EDGE ( 'NONE', *, *, #591, .F. ) ;
#3531=EDGE_CURVE ( 'NONE', #9852, #1879, #615, .T. ) ;
#3548=FACE_OUTER_BOUND ( 'NONE', #13996, .T. ) ;
#3562=DIRECTION ( 'NONE',  ( 1.000000000000000000, 0.000000000000000000, 0.000000000000000000 ) ) ;
#3575=CARTESIAN_POINT ( 'NONE',  ( 3.098410542199072637, -7.060458129626440815, 0.000000000000000000 ) ) ;
#3576=EDGE_LOOP ( 'NONE', ( #16872, #19115, #18912, #10241 ) ) ;
#3580=CARTESIAN_POINT ( 'NONE',  ( 0.1481481481481481122, -4.797713218419819903, 0.000000000000000000 ) ) ;
#3599=EDGE_LOOP ( 'NONE', ( #8081, #7821, #19142, #10554 ) ) ;
#3604=ORIENTED_EDGE ( 'NONE', *, *, #7528, .F. ) ;
#3618=ORIENTED_EDGE ( 'NONE', *, *, #11802, .F. ) ;
#3631=DIRECTION ( 'NONE',  ( 1.000000000000000000, 0.000000000000000000, 0.000000000000000000 ) ) ;
#3639=DIRECTION ( 'NONE',  ( 0.000000000000000000, 0.000000000000000000, 1.000000000000000000 ) ) ;
#3651=LINE ( 'NONE', #9611, #3450 ) ;
#3666=LINE ( 'NONE', #12679, #14427 ) ;
#3682=FACE_OUTER_BOUND ( 'NONE', #14626, .T. ) ;
#3694=ADVANCED_FACE ( 'NONE', ( #5714 ), #2690, .F. ) ;
#3729=CARTESIAN_POINT ( 'NONE',  ( 4.799999999999999822, 0.000000000000000000, -1.000000000000000000 ) ) ;
#3741=LINE ( 'NONE', #18275, #14641 ) ;
#3809=ORIENTED_EDGE ( 'NONE', *, *, #525, .T. ) ;
#3855=DIRECTION ( 'NONE',  ( 1.000000000000000000, 0.000000000000000000, 0.000000000000000000 ) ) ;
#3882=AXIS2_PLACEMENT_3D ( 'NONE', #2226, #6713, #13871 ) ;
#3968=FACE_OUTER_BOUND ( 'NONE', #9669, .T. ) ;
#4071=AXIS2_PLACEMENT_3D ( 'NONE', #11128, #3249, #9014 ) ;
#4078=DIRECTION ( 'NONE',  ( -0.000000000000000000, -0.000000000000000000, -1.000000000000000000 ) ) ;
#4089=VERTEX_POINT ( 'NONE', #13830 ) ;
#4108=VECTOR ( 'NONE', #4801, 1000.000000000000000 ) ;
#4161=ORIENTED_EDGE ( 'NONE', *, *, #12082, .F. ) ;
#4190=ORIENTED_EDGE ( 'NONE', *, *, #3531, .T. ) ;
#4200=AXIS2_PLACEMENT_3D ( 'NONE', #17803, #234, #3096 ) ;
#4203=CARTESIAN_POINT ( 'NONE',  ( 3.098410542199072637, -7.060458129626440815, -1.000000000000000000 ) ) ;
#4257=ORIENTED_EDGE ( 'NONE', *, *, #10349, .T. ) ;
#4301=SURFACE_STYLE_USAGE ( .BOTH. , #11738 ) ;
#4304=DIRECTION ( 'NONE',  ( 0.03086419753086420623, -0.9995235871707959241, 0.000000000000000000 ) ) ;
#4330=CARTESIAN_POINT ( 'NONE',  ( -2.595115354961444076, -7.673029147243174641, -1.000000000000000000 ) ) ;
#4357=ORIENTED_EDGE ( 'NONE', *, *, #12511, .F. ) ;
#4416=ADVANCED_FACE ( 'NONE', ( #6082 ), #3148, .T. ) ;
#4447=DIRECTION ( 'NONE',  ( 0.000000000000000000, 0.000000000000000000, 1.000000000000000000 ) ) ;
#4454=ORIENTED_EDGE ( 'NONE', *, *, #10466, .T. ) ;
#4485=EDGE_CURVE ( 'NONE', #16860, #728, #6109, .T. ) ;
#4557=DIRECTION ( 'NONE',  ( 1.000000000000000000, 0.000000000000000000, 0.000000000000000000 ) ) ;
#4604=VERTEX_POINT ( 'NONE', #7923 ) ;
#4624=AXIS2_PLACEMENT_3D ( 'NONE', #7543, #6080, #16675 ) ;
#4631=VECTOR ( 'NONE', #1305, 999.9999999999998863 ) ;
#4688=DIRECTION ( 'NONE',  ( -0.000000000000000000, -0.000000000000000000, -1.000000000000000000 ) ) ;
#4696=CIRCLE ( 'NONE', #3146, 6.080745460913608902 ) ;
#4727=EDGE_CURVE ( 'NONE', #17826, #8815, #2980, .T. ) ;
#4748=EDGE_CURVE ( 'NONE', #2946, #11693, #9675, .T. ) ;
#4772=DIRECTION ( 'NONE',  ( -0.000000000000000000, -0.000000000000000000, -1.000000000000000000 ) ) ;
#4774=ORIENTED_EDGE ( 'NONE', *, *, #19004, .T. ) ;
#4784=AXIS2_PLACEMENT_3D ( 'NONE', #8985, #7802, #371 ) ;
#4801=DIRECTION ( 'NONE',  ( 0.000000000000000000, 0.000000000000000000, 1.000000000000000000 ) ) ;
#4825=CYLINDRICAL_SURFACE ( 'NONE', #17287, 6.080745460913608902 ) ;
#4839=DIRECTION ( 'NONE',  ( 0.000000000000000000, 0.000000000000000000, 1.000000000000000000 ) ) ;
#4876=CARTESIAN_POINT ( 'NONE',  ( 0.000000000000000000, 0.000000000000000000, -1.000000000000000000 ) ) ;
#4968=CARTESIAN_POINT ( 'NONE',  ( -3.309651814758565180, -5.455921364805393026, 0.000000000000000000 ) ) ;
#5112=DIRECTION ( 'NONE',  ( 1.000000000000000000, 0.000000000000000000, 0.000000000000000000 ) ) ;
#5130=CARTESIAN_POINT ( 'NONE',  ( 2.000000000000000000, -6.429618962271402616, -1.000000000000000000 ) ) ;
#5157=ORIENTED_EDGE ( 'NONE', *, *, #10236, .T. ) ;
#5177=VERTEX_POINT ( 'NONE', #14135 ) ;
#5210=CIRCLE ( 'NONE', #16512, 4.799999999999999822 ) ;
#5223=DIRECTION ( 'NONE',  ( 0.000000000000000000, 0.000000000000000000, 1.000000000000000000 ) ) ;
#5237=VERTEX_POINT ( 'NONE', #16019 ) ;
#5290=CARTESIAN_POINT ( 'NONE',  ( -2.354826896168714434, -6.962563485461402024, -1.000000000000000000 ) ) ;
#5326=CIRCLE ( 'NONE', #15664, 0.7499999999999997780 ) ;
#5328=ORIENTED_EDGE ( 'NONE', *, *, #17793, .T. ) ;
#5335=EDGE_LOOP ( 'NONE', ( #2044, #1647 ) ) ;
#5355=CARTESIAN_POINT ( 'NONE',  ( 0.5000000000000000000, -6.429618962271402616, -1.000000000000000000 ) ) ;
#5357=ORIENTED_EDGE ( 'NONE', *, *, #14178, .T. ) ;
#5378=ADVANCED_FACE ( 'NONE', ( #7569 ), #2974, .F. ) ;
#5394=DIRECTION ( 'NONE',  ( 0.000000000000000000, 0.000000000000000000, 1.000000000000000000 ) ) ;
#5420=EDGE_LOOP ( 'NONE', ( #15567, #10795, #786, #15765 ) ) ;
#5426=ORIENTED_EDGE ( 'NONE', *, *, #7528, .T. ) ;
#5448=EDGE_LOOP ( 'NONE', ( #13879, #1124, #10565, #14704 ) ) ;
#5451=AXIS2_PLACEMENT_3D ( 'NONE', #17683, #11681, #5610 ) ;
#5482=EDGE_CURVE ( 'NONE', #1879, #14662, #7662, .T. ) ;
#5504=CIRCLE ( 'NONE', #11125, 0.7500000000000000000 ) ;
#5519=ORIENTED_EDGE ( 'NONE', *, *, #16002, .F. ) ;
#5523=CARTESIAN_POINT ( 'NONE',  ( 0.000000000000000000, 0.000000000000000000, 0.000000000000000000 ) ) ;
#5540=ORIENTED_EDGE ( 'NONE', *, *, #6305, .F. ) ;
#5547=DIRECTION ( 'NONE',  ( 1.000000000000000000, 0.000000000000000000, 0.000000000000000000 ) ) ;
#5560=ADVANCED_FACE ( 'NONE', ( #3548 ), #4825, .T. ) ;
#5567=CARTESIAN_POINT ( 'NONE',  ( 0.000000000000000000, 0.5192545390863916310, -1.000000000000000000 ) ) ;
#5597=VECTOR ( 'NONE', #7721, 1000.000000000000114 ) ;
#5610=DIRECTION ( 'NONE',  ( 1.000000000000000000, 0.000000000000000000, 0.000000000000000000 ) ) ;
#5617=EDGE_CURVE ( 'NONE', #2130, #11693, #9129, .T. ) ;
#5621=ORIENTED_EDGE ( 'NONE', *, *, #15205, .F. ) ;
#5625=DIRECTION ( 'NONE',  ( 0.000000000000000000, 0.000000000000000000, 1.000000000000000000 ) ) ;
#5641=AXIS2_PLACEMENT_3D ( 'NONE', #7161, #9800, #2582 ) ;
#5659=VECTOR ( 'NONE', #14453, 1000.000000000000000 ) ;
#5691=ADVANCED_FACE ( 'NONE', ( #17663 ), #13140, .F. ) ;
#5714=FACE_OUTER_BOUND ( 'NONE', #3576, .T. ) ;
#5737=EDGE_CURVE ( 'NONE', #10144, #10530, #8431, .T. ) ;
#5754=DIRECTION ( 'NONE',  ( -1.000000000000000000, 0.000000000000000000, 0.000000000000000000 ) ) ;
#5771=FILL_AREA_STYLE ('',( #8809 ) ) ;
#5820=EDGE_CURVE ( 'NONE', #13173, #8527, #15709, .T. ) ;
#5823=DIRECTION ( 'NONE',  ( 1.000000000000000000, 0.000000000000000000, 0.000000000000000000 ) ) ;
#5923=ORIENTED_EDGE ( 'NONE', *, *, #17326, .F. ) ;
#5925=AXIS2_PLACEMENT_3D ( 'NONE', #853, #2249, #5547 ) ;
#5945=ORIENTED_EDGE ( 'NONE', *, *, #591, .T. ) ;
#5954=EDGE_LOOP ( 'NONE', ( #16878, #157 ) ) ;
#5965=PLANE ( 'NONE',  #13947 ) ;
#6002=ORIENTED_EDGE ( 'NONE', *, *, #17573, .T. ) ;
#6035=CARTESIAN_POINT ( 'NONE',  ( -4.799999999999999822, 5.878304635907294211E-16, -1.000000000000000000 ) ) ;
#6080=DIRECTION ( 'NONE',  ( -0.9914448613738102711, -0.1305261922200524338, 0.000000000000000000 ) ) ;
#6082=FACE_OUTER_BOUND ( 'NONE', #17872, .T. ) ;
#6109=CIRCLE ( 'NONE', #14233, 8.099999999999999645 ) ;
#6136=CARTESIAN_POINT ( 'NONE',  ( 0.000000000000000000, 0.000000000000000000, 0.000000000000000000 ) ) ;
#6159=FACE_OUTER_BOUND ( 'NONE', #17245, .T. ) ;
#6198=DIRECTION ( 'NONE',  ( 0.000000000000000000, 0.000000000000000000, 1.000000000000000000 ) ) ;
#6213=AXIS2_PLACEMENT_3D ( 'NONE', #18139, #8710, #4304 ) ;
#6295=CARTESIAN_POINT ( 'NONE',  ( 0.000000000000000000, 0.000000000000000000, -1.000000000000000000 ) ) ;
#6305=EDGE_CURVE ( 'NONE', #2946, #4089, #18512, .T. ) ;
#6350=LINE ( 'NONE', #9567, #5597 ) ;
#6379=CARTESIAN_POINT ( 'NONE',  ( 0.000000000000000000, 0.5192545390863916310, 0.000000000000000000 ) ) ;
#6447=FACE_OUTER_BOUND ( 'NONE', #15532, .T. ) ;
#6451=CARTESIAN_POINT ( 'NONE',  ( 6.080745460913608902, 0.5192545390863916310, 0.000000000000000000 ) ) ;
#6462=VECTOR ( 'NONE', #1711, 1000.000000000000000 ) ;
#6473=DIRECTION ( 'NONE',  ( 1.000000000000000000, 0.000000000000000000, 0.000000000000000000 ) ) ;
#6479=VECTOR ( 'NONE', #912, 1000.000000000000000 ) ;
#6484=DIRECTION ( 'NONE',  ( 0.000000000000000000, 0.000000000000000000, 1.000000000000000000 ) ) ;
#6544=UNCERTAINTY_MEASURE_WITH_UNIT (LENGTH_MEASURE( 1.000000000000000082E-05 ), #7590, 'distance_accuracy_value', 'NONE');
#6566=CARTESIAN_POINT ( 'NONE',  ( -0.5000000000000000000, -6.429618962271402616, -1.000000000000000000 ) ) ;
#6578=CYLINDRICAL_SURFACE ( 'NONE', #14736, 6.080745460913608902 ) ;
#6623=CIRCLE ( 'NONE', #11630, 4.799999999999999822 ) ;
#6643=VERTEX_POINT ( 'NONE', #5355 ) ;
#6682=DIRECTION ( 'NONE',  ( 0.000000000000000000, 0.000000000000000000, 1.000000000000000000 ) ) ;
#6689=CARTESIAN_POINT ( 'NONE',  ( 0.000000000000000000, 0.000000000000000000, -1.000000000000000000 ) ) ;
#6713=DIRECTION ( 'NONE',  ( 0.000000000000000000, 0.000000000000000000, 1.000000000000000000 ) ) ;
#6742=PRODUCT_DEFINITION ( 'UNKNOWN', '', #2301, #18539 ) ;
#6759=CARTESIAN_POINT ( 'NONE',  ( -2.354826896168714434, -6.962563485461402024, -1.000000000000000000 ) ) ;
#6760=FACE_OUTER_BOUND ( 'NONE', #11036, .T. ) ;
#6787=CARTESIAN_POINT ( 'NONE',  ( -5.686050877451574337, -5.768780236673276995, -1.000000000000000000 ) ) ;
#6852=ORIENTED_EDGE ( 'NONE', *, *, #12523, .T. ) ;
#6901=PLANE ( 'NONE',  #16633 ) ;
#6941=CARTESIAN_POINT ( 'NONE',  ( -6.080745460913608902, 0.5192545390863924082, -1.000000000000000000 ) ) ;
#6943=DIRECTION ( 'NONE',  ( 0.000000000000000000, 0.000000000000000000, 1.000000000000000000 ) ) ;
#6967=CARTESIAN_POINT ( 'NONE',  ( 1.250000000000000000, -6.429618962271402616, 0.000000000000000000 ) ) ;
#6968=PLANE ( 'NONE',  #653 ) ;
#6970=ORIENTED_EDGE ( 'NONE', *, *, #12883, .T. ) ;
#6971=ORIENTED_EDGE ( 'NONE', *, *, #5737, .T. ) ;
#6977=ORIENTED_EDGE ( 'NONE', *, *, #12523, .F. ) ;
#6995=CARTESIAN_POINT ( 'NONE',  ( -2.595115354961444076, -7.673029147243174641, 0.000000000000000000 ) ) ;
#7043=SURFACE_STYLE_FILL_AREA ( #5771 ) ;
#7114=EDGE_CURVE ( 'NONE', #40, #18188, #1718, .T. ) ;
#7161=CARTESIAN_POINT ( 'NONE',  ( -5.686050877451574337, -5.768780236673276995, -1.000000000000000000 ) ) ;
#7166=EDGE_CURVE ( 'NONE', #8318, #2130, #3666, .T. ) ;
#7185=AXIS2_PLACEMENT_3D ( 'NONE', #17039, #8092, #12509 ) ;
#7219=ORIENTED_EDGE ( 'NONE', *, *, #2388, .T. ) ;
#7243=( NAMED_UNIT ( * ) SI_UNIT ( $, .STERADIAN. ) SOLID_ANGLE_UNIT ( ) );
#7256=AXIS2_PLACEMENT_3D ( 'NONE', #11267, #17472, #17576 ) ;
#7270=ORIENTED_EDGE ( 'NONE', *, *, #880, .F. ) ;
#7292=DIRECTION ( 'NONE',  ( 0.000000000000000000, 0.000000000000000000, 1.000000000000000000 ) ) ;
#7349=DIRECTION ( 'NONE',  ( 0.9995235871707960351, -0.03086419753086420970, 0.000000000000000000 ) ) ;
#7372=EDGE_CURVE ( 'NONE', #3206, #11016, #15132, .T. ) ;
#7408=LINE ( 'NONE', #19209, #19104 ) ;
#7482=CARTESIAN_POINT ( 'NONE',  ( 0.2499999999999966416, -8.096141056083448362, -1.000000000000000000 ) ) ;
#7528=EDGE_CURVE ( 'NONE', #3206, #17826, #11892, .T. ) ;
#7540=EDGE_LOOP ( 'NONE', ( #13888, #14787, #4257, #1669 ) ) ;
#7543=CARTESIAN_POINT ( 'NONE',  ( -3.309651814758565180, -5.455921364805393026, -1.000000000000000000 ) ) ;
#7569=FACE_OUTER_BOUND ( 'NONE', #16394, .T. ) ;
#7575=AXIS2_PLACEMENT_3D ( 'NONE', #6759, #16255, #10068 ) ;
#7582=AXIS2_PLACEMENT_3D ( 'NONE', #17517, #4078, #10044 ) ;
#7586=CARTESIAN_POINT ( 'NONE',  ( -3.098410542199071749, -7.060458129626440815, -1.000000000000000000 ) ) ;
#7590=( LENGTH_UNIT ( ) NAMED_UNIT ( * ) SI_UNIT ( .MILLI., .METRE. ) );
#7662=LINE ( 'NONE', #13643, #10691 ) ;
#7721=DIRECTION ( 'NONE',  ( 0.03086419753086420623, 0.9995235871707959241, -0.000000000000000000 ) ) ;
#7737=ADVANCED_FACE ( 'NONE', ( #18767 ), #2948, .F. ) ;
#7745=CYLINDRICAL_SURFACE ( 'NONE', #17804, 0.7499999999999997780 ) ;
#7759=CYLINDRICAL_SURFACE ( 'NONE', #13390, 8.099999999999999645 ) ;
#7765=DIRECTION ( 'NONE',  ( 0.000000000000000000, 0.000000000000000000, 1.000000000000000000 ) ) ;
#7802=DIRECTION ( 'NONE',  ( -0.000000000000000000, -0.000000000000000000, -1.000000000000000000 ) ) ;
#7821=ORIENTED_EDGE ( 'NONE', *, *, #7166, .T. ) ;
#7872=CARTESIAN_POINT ( 'NONE',  ( 1.250000000000000000, -6.429618962271402616, -1.000000000000000000 ) ) ;
#7889=ORIENTED_EDGE ( 'NONE', *, *, #2799, .T. ) ;
#7923=CARTESIAN_POINT ( 'NONE',  ( 0.2499999999999966416, -8.096141056083448362, -1.000000000000000000 ) ) ;
#7950=ADVANCED_FACE ( 'NONE', ( #6447 ), #12428, .T. ) ;
#7965=CARTESIAN_POINT ( 'NONE',  ( -2.000000000000000000, -6.429618962271402616, -1.000000000000000000 ) ) ;
#7969=AXIS2_PLACEMENT_3D ( 'NONE', #12827, #14384, #19023 ) ;
#7993=DIRECTION ( 'NONE',  ( 1.000000000000000000, 0.000000000000000000, 0.000000000000000000 ) ) ;
#8049=CARTESIAN_POINT ( 'NONE',  ( -0.1481481481481481122, -4.797713218419819903, -1.000000000000000000 ) ) ;
#8068=MECHANICAL_DESIGN_GEOMETRIC_PRESENTATION_REPRESENTATION('',(#2780),#19415);
#8081=ORIENTED_EDGE ( 'NONE', *, *, #16962, .T. ) ;
#8092=DIRECTION ( 'NONE',  ( 0.000000000000000000, 0.000000000000000000, 1.000000000000000000 ) ) ;
#8112=CARTESIAN_POINT ( 'NONE',  ( 0.000000000000000000, 0.000000000000000000, 0.000000000000000000 ) ) ;
#8131=CYLINDRICAL_SURFACE ( 'NONE', #1284, 6.080745460913608902 ) ;
#8134=CIRCLE ( 'NONE', #15351, 6.080745460913608902 ) ;
#8148=CARTESIAN_POINT ( 'NONE',  ( -4.799999999999999822, 5.878304635907294211E-16, 0.000000000000000000 ) ) ;
#8173=ORIENTED_EDGE ( 'NONE', *, *, #417, .T. ) ;
#8187=PRODUCT_DEFINITION_SHAPE ( 'NONE', 'NONE',  #6742 ) ;
#8267=VERTEX_POINT ( 'NONE', #17935 ) ;
#8318=VERTEX_POINT ( 'NONE', #16163 ) ;
#8357=DIRECTION ( 'NONE',  ( 0.000000000000000000, 0.000000000000000000, 1.000000000000000000 ) ) ;
#8370=CYLINDRICAL_SURFACE ( 'NONE', #8677, 0.7500000000000000000 ) ;
#8385=VERTEX_POINT ( 'NONE', #18026 ) ;
#8431=LINE ( 'NONE', #14409, #19183 ) ;
#8435=EDGE_CURVE ( 'NONE', #10530, #16860, #13686, .T. ) ;
#8448=CARTESIAN_POINT ( 'NONE',  ( 0.000000000000000000, 0.5192545390863916310, -1.000000000000000000 ) ) ;
#8484=DIRECTION ( 'NONE',  ( -0.000000000000000000, -0.000000000000000000, -1.000000000000000000 ) ) ;
#8527=VERTEX_POINT ( 'NONE', #14064 ) ;
#8599=ORIENTED_EDGE ( 'NONE', *, *, #773, .F. ) ;
#8652=DIRECTION ( 'NONE',  ( 0.000000000000000000, 0.000000000000000000, 1.000000000000000000 ) ) ;
#8663=DIRECTION ( 'NONE',  ( 1.000000000000000000, 0.000000000000000000, 0.000000000000000000 ) ) ;
#8677=AXIS2_PLACEMENT_3D ( 'NONE', #14351, #10614, #4557 ) ;
#8709=DIRECTION ( 'NONE',  ( 0.000000000000000000, 0.000000000000000000, 1.000000000000000000 ) ) ;
#8710=DIRECTION ( 'NONE',  ( -0.9995235871707960351, -0.03086419753086420970, 0.000000000000000000 ) ) ;
#8775=AXIS2_PLACEMENT_3D ( 'NONE', #6136, #12107, #253 ) ;
#8776=DIRECTION ( 'NONE',  ( 0.000000000000000000, 0.000000000000000000, 1.000000000000000000 ) ) ;
#8788=CARTESIAN_POINT ( 'NONE',  ( 2.354826896168714434, -6.962563485461402024, -1.000000000000000000 ) ) ;
#8790=MANIFOLD_SOLID_BREP ( 'Body', #14303 ) ;
#8809=FILL_AREA_STYLE_COLOUR ( '', #12463 ) ;
#8815=VERTEX_POINT ( 'NONE', #6035 ) ;
#8819=CYLINDRICAL_SURFACE ( 'NONE', #3166, 8.099999999999999645 ) ;
#8834=DIRECTION ( 'NONE',  ( 0.000000000000000000, 0.000000000000000000, 1.000000000000000000 ) ) ;
#8880=DIRECTION ( 'NONE',  ( 0.000000000000000000, 0.000000000000000000, 1.000000000000000000 ) ) ;
#8914=CARTESIAN_POINT ( 'NONE',  ( -0.1481481481481481122, -4.797713218419819903, -1.000000000000000000 ) ) ;
#8945=ORIENTED_EDGE ( 'NONE', *, *, #12511, .T. ) ;
#8964=CARTESIAN_POINT ( 'NONE',  ( -4.799999999999999822, 5.878304635907294211E-16, -1.000000000000000000 ) ) ;
#8974=VERTEX_POINT ( 'NONE', #8148 ) ;
#8985=CARTESIAN_POINT ( 'NONE',  ( 0.000000000000000000, 0.000000000000000000, 0.000000000000000000 ) ) ;
#8999=EDGE_LOOP ( 'NONE', ( #2140, #18326, #17694, #12584 ) ) ;
#9007=AXIS2_PLACEMENT_3D ( 'NONE', #6787, #12771, #3855 ) ;
#9014=DIRECTION ( 'NONE',  ( 1.000000000000000000, 0.000000000000000000, 0.000000000000000000 ) ) ;
#9087=DIRECTION ( 'NONE',  ( 1.000000000000000000, 0.000000000000000000, -0.000000000000000000 ) ) ;
#9121=EDGE_LOOP ( 'NONE', ( #13566, #5519 ) ) ;
#9129=CIRCLE ( 'NONE', #11626, 6.080745460913608902 ) ;
#9135=CARTESIAN_POINT ( 'NONE',  ( 1.250000000000000000, -6.429618962271402616, -1.000000000000000000 ) ) ;
#9216=LINE ( 'NONE', #10590, #944 ) ;
#9306=ORIENTED_EDGE ( 'NONE', *, *, #16359, .T. ) ;
#9397=CIRCLE ( 'NONE', #12526, 2.396904916527700102 ) ;
#9405=AXIS2_PLACEMENT_3D ( 'NONE', #11983, #8652, #2891 ) ;
#9496=CARTESIAN_POINT ( 'NONE',  ( 0.2499999999999966416, -8.096141056083448362, 0.000000000000000000 ) ) ;
#9499=FACE_OUTER_BOUND ( 'NONE', #3599, .T. ) ;
#9567=CARTESIAN_POINT ( 'NONE',  ( -0.1481481481481481122, -4.797713218419819903, 0.000000000000000000 ) ) ;
#9606=CIRCLE ( 'NONE', #11137, 8.099999999999999645 ) ;
#9610=AXIS2_PLACEMENT_3D ( 'NONE', #17653, #8709, #1075 ) ;
#9611=CARTESIAN_POINT ( 'NONE',  ( -3.309651814758565180, -5.455921364805393026, -1.000000000000000000 ) ) ;
#9648=CYLINDRICAL_SURFACE ( 'NONE', #3882, 2.396904916527699214 ) ;
#9669=EDGE_LOOP ( 'NONE', ( #5945, #4454, #2344, #18977, #12980, #3809, #17928, #18242, #3089, #17234, #4774, #18286, #11446, #7219, #11544, #17429 ) ) ;
#9675=LINE ( 'NONE', #6941, #18016 ) ;
#9694=DIRECTION ( 'NONE',  ( 0.000000000000000000, 0.000000000000000000, 1.000000000000000000 ) ) ;
#9783=DIRECTION ( 'NONE',  ( 1.000000000000000000, 0.000000000000000000, 0.000000000000000000 ) ) ;
#9800=DIRECTION ( 'NONE',  ( 0.000000000000000000, 0.000000000000000000, 1.000000000000000000 ) ) ;
#9852=VERTEX_POINT ( 'NONE', #19335 ) ;
#9907=AXIS2_PLACEMENT_3D ( 'NONE', #16224, #18093, #19288 ) ;
#9925=CIRCLE ( 'NONE', #9610, 0.7500000000000000000 ) ;
#9971=ORIENTED_EDGE ( 'NONE', *, *, #5482, .T. ) ;
#9974=( NAMED_UNIT ( * ) PLANE_ANGLE_UNIT ( ) SI_UNIT ( $, .RADIAN. ) );
#10026=AXIS2_PLACEMENT_3D ( 'NONE', #17824, #19310, #10345 ) ;
#10044=DIRECTION ( 'NONE',  ( 1.000000000000000000, 0.000000000000000000, 0.000000000000000000 ) ) ;
#10068=DIRECTION ( 'NONE',  ( 1.000000000000000000, 0.000000000000000000, 0.000000000000000000 ) ) ;
#10112=CARTESIAN_POINT ( 'NONE',  ( 2.000000000000000000, -6.429618962271402616, -1.000000000000000000 ) ) ;
#10131=DIRECTION ( 'NONE',  ( -0.000000000000000000, -0.000000000000000000, -1.000000000000000000 ) ) ;
#10134=CARTESIAN_POINT ( 'NONE',  ( -0.2500000000000000000, -8.096141056083446585, -1.000000000000000000 ) ) ;
#10144=VERTEX_POINT ( 'NONE', #17346 ) ;
#10153=ORIENTED_EDGE ( 'NONE', *, *, #4727, .F. ) ;
#10165=FACE_BOUND ( 'NONE', #5954, .T. ) ;
#10236=EDGE_CURVE ( 'NONE', #17826, #11915, #17922, .T. ) ;
#10241=ORIENTED_EDGE ( 'NONE', *, *, #2274, .T. ) ;
#10267=( NAMED_UNIT ( * ) SI_UNIT ( $, .STERADIAN. ) SOLID_ANGLE_UNIT ( ) );
#10280=DIRECTION ( 'NONE',  ( 1.000000000000000000, 0.000000000000000000, 0.000000000000000000 ) ) ;
#10310=CIRCLE ( 'NONE', #4071, 6.080745460913608902 ) ;
#10344=ORIENTED_EDGE ( 'NONE', *, *, #5737, .F. ) ;
#10345=DIRECTION ( 'NONE',  ( 1.000000000000000000, 0.000000000000000000, 0.000000000000000000 ) ) ;
#10346=VECTOR ( 'NONE', #16179, 1000.000000000000000 ) ;
#10349=EDGE_CURVE ( 'NONE', #16533, #3206, #2211, .T. ) ;
#10359=AXIS2_PLACEMENT_3D ( 'NONE', #2871, #8834, #16191 ) ;
#10385=CARTESIAN_POINT ( 'NONE',  ( 3.309651814758564736, -5.455921364805393026, -1.000000000000000000 ) ) ;
#10398=ORIENTED_EDGE ( 'NONE', *, *, #4485, .F. ) ;
#10415=EDGE_LOOP ( 'NONE', ( #10418, #4357, #14372, #9306 ) ) ;
#10418=ORIENTED_EDGE ( 'NONE', *, *, #10579, .F. ) ;
#10427=CARTESIAN_POINT ( 'NONE',  ( -3.309651814758565180, -5.455921364805393026, -1.000000000000000000 ) ) ;
#10466=EDGE_CURVE ( 'NONE', #8974, #17434, #16938, .T. ) ;
#10530=VERTEX_POINT ( 'NONE', #3580 ) ;
#10554=ORIENTED_EDGE ( 'NONE', *, *, #13386, .F. ) ;
#10559=PLANE ( 'NONE',  #6213 ) ;
#10565=ORIENTED_EDGE ( 'NONE', *, *, #17326, .T. ) ;
#10579=EDGE_CURVE ( 'NONE', #11530, #15909, #9397, .T. ) ;
#10590=CARTESIAN_POINT ( 'NONE',  ( -3.309651814758565180, -5.455921364805393026, -1.000000000000000000 ) ) ;
#10614=DIRECTION ( 'NONE',  ( 0.000000000000000000, 0.000000000000000000, 1.000000000000000000 ) ) ;
#10691=VECTOR ( 'NONE', #6198, 1000.000000000000000 ) ;
#10711=EDGE_CURVE ( 'NONE', #6643, #5237, #18691, .T. ) ;
#10756=ADVANCED_FACE ( 'NONE', ( #929, #16128, #3968 ), #6901, .T. ) ;
#10767=DIRECTION ( 'NONE',  ( 0.000000000000000000, 0.000000000000000000, 1.000000000000000000 ) ) ;
#10795=ORIENTED_EDGE ( 'NONE', *, *, #14178, .F. ) ;
#10845=LINE ( 'NONE', #4968, #14989 ) ;
#10892=VERTEX_POINT ( 'NONE', #14935 ) ;
#10941=DIRECTION ( 'NONE',  ( 0.1305261922200524616, -0.9914448613738103822, 0.000000000000000000 ) ) ;
#11002=DIRECTION ( 'NONE',  ( 0.1305261922200524616, 0.9914448613738103822, -0.000000000000000000 ) ) ;
#11016=VERTEX_POINT ( 'NONE', #510 ) ;
#11036=EDGE_LOOP ( 'NONE', ( #17309, #825, #7889, #6002 ) ) ;
#11078=CARTESIAN_POINT ( 'NONE',  ( 0.000000000000000000, 0.5192545390863916310, -1.000000000000000000 ) ) ;
#11081=DIRECTION ( 'NONE',  ( 0.03086419753086420623, -0.9995235871707959241, 0.000000000000000000 ) ) ;
#11114=CARTESIAN_POINT ( 'NONE',  ( -4.078421086530219064, -3.990950201428956845, 0.000000000000000000 ) ) ;
#11125=AXIS2_PLACEMENT_3D ( 'NONE', #14678, #16459, #3130 ) ;
#11128=CARTESIAN_POINT ( 'NONE',  ( 0.000000000000000000, 0.5192545390863916310, 0.000000000000000000 ) ) ;
#11137=AXIS2_PLACEMENT_3D ( 'NONE', #15700, #2279, #11660 ) ;
#11173=DIRECTION ( 'NONE',  ( 1.000000000000000000, 0.000000000000000000, 0.000000000000000000 ) ) ;
#11203=( GEOMETRIC_REPRESENTATION_CONTEXT ( 3 ) GLOBAL_UNCERTAINTY_ASSIGNED_CONTEXT ( ( #14794 ) ) GLOBAL_UNIT_ASSIGNED_CONTEXT ( ( #11448, #9974, #7243 ) ) REPRESENTATION_CONTEXT ( 'NONE', 'WORKASPACE' ) );
#11232=CYLINDRICAL_SURFACE ( 'NONE', #5925, 4.799999999999999822 ) ;
#11234=ORIENTED_EDGE ( 'NONE', *, *, #3385, .T. ) ;
#11267=CARTESIAN_POINT ( 'NONE',  ( -1.250000000000000000, -6.429618962271402616, -1.000000000000000000 ) ) ;
#11274=DIRECTION ( 'NONE',  ( 0.000000000000000000, 0.000000000000000000, 1.000000000000000000 ) ) ;
#11289=CARTESIAN_POINT ( 'NONE',  ( -1.250000000000000000, -6.429618962271402616, -1.000000000000000000 ) ) ;
#11316=ORIENTED_EDGE ( 'NONE', *, *, #417, .F. ) ;
#11368=DIRECTION ( 'NONE',  ( 0.000000000000000000, 0.000000000000000000, 1.000000000000000000 ) ) ;
#11372=CARTESIAN_POINT ( 'NONE',  ( 3.309651814758565180, -5.455921364805393026, -1.000000000000000000 ) ) ;
#11446=ORIENTED_EDGE ( 'NONE', *, *, #13760, .T. ) ;
#11448=( LENGTH_UNIT ( ) NAMED_UNIT ( * ) SI_UNIT ( .MILLI., .METRE. ) );
#11500=ORIENTED_EDGE ( 'NONE', *, *, #10711, .T. ) ;
#11530=VERTEX_POINT ( 'NONE', #11114 ) ;
#11544=ORIENTED_EDGE ( 'NONE', *, *, #1800, .T. ) ;
#11547=LINE ( 'NONE', #14493, #13070 ) ;
#11604=CARTESIAN_POINT ( 'NONE',  ( 0.000000000000000000, 0.000000000000000000, -1.000000000000000000 ) ) ;
#11626=AXIS2_PLACEMENT_3D ( 'NONE', #6379, #3639, #15596 ) ;
#11630=AXIS2_PLACEMENT_3D ( 'NONE', #4876, #12409, #7993 ) ;
#11660=DIRECTION ( 'NONE',  ( 1.000000000000000000, 0.000000000000000000, 0.000000000000000000 ) ) ;
#11681=DIRECTION ( 'NONE',  ( 0.000000000000000000, 0.000000000000000000, 1.000000000000000000 ) ) ;
#11693=VERTEX_POINT ( 'NONE', #17512 ) ;
#11701=VECTOR ( 'NONE', #11002, 999.9999999999998863 ) ;
#11708=LINE ( 'NONE', #8964, #1892 ) ;
#11738=SURFACE_SIDE_STYLE ('',( #7043 ) ) ;
#11802=EDGE_CURVE ( 'NONE', #8815, #2828, #5210, .T. ) ;
#11834=ADVANCED_FACE ( 'NONE', ( #2419 ), #8370, .F. ) ;
#11869=AXIS2_PLACEMENT_3D ( 'NONE', #17609, #5625, #5823 ) ;
#11892=LINE ( 'NONE', #17903, #18076 ) ;
#11897=( NAMED_UNIT ( * ) SI_UNIT ( $, .STERADIAN. ) SOLID_ANGLE_UNIT ( ) );
#11915=VERTEX_POINT ( 'NONE', #15130 ) ;
#11926=EDGE_CURVE ( 'NONE', #5237, #18188, #19032, .T. ) ;
#11935=SHAPE_REPRESENTATION ( 'circlip for shafts normal_din_Circlip DIN 471 - 10 x 1', ( #10359 ), #11203 ) ;
#11983=CARTESIAN_POINT ( 'NONE',  ( 0.000000000000000000, 0.5192545390863916310, 0.000000000000000000 ) ) ;
#11994=ORIENTED_EDGE ( 'NONE', *, *, #16962, .F. ) ;
#12024=DIRECTION ( 'NONE',  ( 0.000000000000000000, 0.000000000000000000, 1.000000000000000000 ) ) ;
#12082=EDGE_CURVE ( 'NONE', #40, #6643, #2429, .T. ) ;
#12107=DIRECTION ( 'NONE',  ( -0.000000000000000000, -0.000000000000000000, -1.000000000000000000 ) ) ;
#12142=CIRCLE ( 'NONE', #9007, 2.396904916527700102 ) ;
#12241=LINE ( 'NONE', #18247, #4108 ) ;
#12253=DIRECTION ( 'NONE',  ( 1.000000000000000000, 0.000000000000000000, 0.000000000000000000 ) ) ;
#12348=ORIENTED_EDGE ( 'NONE', *, *, #7114, .T. ) ;
#12350=DIRECTION ( 'NONE',  ( 0.1305261922200524616, -0.9914448613738103822, 0.000000000000000000 ) ) ;
#12378=CYLINDRICAL_SURFACE ( 'NONE', #18114, 4.799999999999999822 ) ;
#12398=EDGE_CURVE ( 'NONE', #14377, #14662, #16199, .T. ) ;
#12409=DIRECTION ( 'NONE',  ( -0.000000000000000000, -0.000000000000000000, -1.000000000000000000 ) ) ;
#12428=PLANE ( 'NONE',  #4624 ) ;
#12463=COLOUR_RGB ( '',1.000000000000000000, 0.9490196078431372140, 0.9098039215686274384 ) ;
#12469=CARTESIAN_POINT ( 'NONE',  ( 3.309651814758565180, -5.455921364805393026, -1.000000000000000000 ) ) ;
#12483=VECTOR ( 'NONE', #7292, 1000.000000000000000 ) ;
#12487=CARTESIAN_POINT ( 'NONE',  ( -5.686050877451574337, -5.768780236673276995, 0.000000000000000000 ) ) ;
#12509=DIRECTION ( 'NONE',  ( 1.000000000000000000, 0.000000000000000000, 0.000000000000000000 ) ) ;
#12511=EDGE_CURVE ( 'NONE', #4089, #11530, #11547, .T. ) ;
#12523=EDGE_CURVE ( 'NONE', #6643, #40, #9925, .T. ) ;
#12526=AXIS2_PLACEMENT_3D ( 'NONE', #12487, #4772, #18405 ) ;
#12584=ORIENTED_EDGE ( 'NONE', *, *, #17114, .F. ) ;
#12672=DIRECTION ( 'NONE',  ( 0.000000000000000000, 0.000000000000000000, 1.000000000000000000 ) ) ;
#12679=CARTESIAN_POINT ( 'NONE',  ( 6.080745460913608902, 0.5192545390863916310, -1.000000000000000000 ) ) ;
#12687=CARTESIAN_POINT ( 'NONE',  ( -3.309651814758565180, -5.455921364805393026, 0.000000000000000000 ) ) ;
#12689=CARTESIAN_POINT ( 'NONE',  ( 0.5000000000000000000, -6.429618962271402616, -1.000000000000000000 ) ) ;
#12717=ORIENTED_EDGE ( 'NONE', *, *, #7114, .F. ) ;
#12723=AXIS2_PLACEMENT_3D ( 'NONE', #11289, #14795, #10280 ) ;
#12740=EDGE_CURVE ( 'NONE', #10144, #4604, #3741, .T. ) ;
#12742=CARTESIAN_POINT ( 'NONE',  ( 0.000000000000000000, 0.5192545390863916310, -1.000000000000000000 ) ) ;
#12755=DIRECTION ( 'NONE',  ( 1.000000000000000000, 0.000000000000000000, 0.000000000000000000 ) ) ;
#12764=ADVANCED_FACE ( 'NONE', ( #16896 ), #17179, .F. ) ;
#12771=DIRECTION ( 'NONE',  ( -0.000000000000000000, -0.000000000000000000, -1.000000000000000000 ) ) ;
#12774=VECTOR ( 'NONE', #432, 1000.000000000000000 ) ;
#12827=CARTESIAN_POINT ( 'NONE',  ( 0.000000000000000000, 0.000000000000000000, -1.000000000000000000 ) ) ;
#12850=CIRCLE ( 'NONE', #9405, 6.080745460913608902 ) ;
#12855=EDGE_LOOP ( 'NONE', ( #17332, #16961, #8945, #13727 ) ) ;
#12856=VECTOR ( 'NONE', #9694, 1000.000000000000000 ) ;
#12883=EDGE_CURVE ( 'NONE', #18188, #5237, #13084, .T. ) ;
#12889=DIRECTION ( 'NONE',  ( 1.000000000000000000, 0.000000000000000000, -0.000000000000000000 ) ) ;
#12906=ORIENTED_EDGE ( 'NONE', *, *, #13386, .T. ) ;
#12936=DIRECTION ( 'NONE',  ( 1.000000000000000000, 0.000000000000000000, 0.000000000000000000 ) ) ;
#12980=ORIENTED_EDGE ( 'NONE', *, *, #4485, .T. ) ;
#12999=ORIENTED_EDGE ( 'NONE', *, *, #1368, .T. ) ;
#13024=( NAMED_UNIT ( * ) PLANE_ANGLE_UNIT ( ) SI_UNIT ( $, .RADIAN. ) );
#13035=DIRECTION ( 'NONE',  ( 1.000000000000000000, 0.000000000000000000, 0.000000000000000000 ) ) ;
#13046=DIRECTION ( 'NONE',  ( 0.000000000000000000, 0.000000000000000000, 1.000000000000000000 ) ) ;
#13070=VECTOR ( 'NONE', #873, 1000.000000000000000 ) ;
#13084=CIRCLE ( 'NONE', #14962, 0.7500000000000000000 ) ;
#13134=CIRCLE ( 'NONE', #7185, 0.7500000000000000000 ) ;
#13138=DIRECTION ( 'NONE',  ( 1.000000000000000000, 0.000000000000000000, 0.000000000000000000 ) ) ;
#13140=CYLINDRICAL_SURFACE ( 'NONE', #5641, 2.396904916527700102 ) ;
#13173=VERTEX_POINT ( 'NONE', #14908 ) ;
#13176=ORIENTED_EDGE ( 'NONE', *, *, #16359, .F. ) ;
#13262=CIRCLE ( 'NONE', #4200, 8.099999999999999645 ) ;
#13266=AXIS2_PLACEMENT_3D ( 'NONE', #9135, #4447, #15213 ) ;
#13346=ADVANCED_FACE ( 'NONE', ( #13817 ), #7745, .T. ) ;
#13386=EDGE_CURVE ( 'NONE', #10892, #8385, #15875, .T. ) ;
#13390=AXIS2_PLACEMENT_3D ( 'NONE', #6295, #5394, #13138 ) ;
#13497=DIRECTION ( 'NONE',  ( 1.000000000000000000, 0.000000000000000000, 0.000000000000000000 ) ) ;
#13542=CIRCLE ( 'NONE', #17629, 2.396904916527699214 ) ;
#13557=ORIENTED_EDGE ( 'NONE', *, *, #16593, .F. ) ;
#13566=ORIENTED_EDGE ( 'NONE', *, *, #2274, .F. ) ;
#13610=EDGE_CURVE ( 'NONE', #9852, #14377, #17652, .T. ) ;
#13643=CARTESIAN_POINT ( 'NONE',  ( 3.309651814758564736, -5.455921364805393026, -1.000000000000000000 ) ) ;
#13686=LINE ( 'NONE', #18230, #243 ) ;
#13709=ORIENTED_EDGE ( 'NONE', *, *, #5617, .F. ) ;
#13724=CARTESIAN_POINT ( 'NONE',  ( 2.354826896168714434, -6.962563485461402024, -1.000000000000000000 ) ) ;
#13727=ORIENTED_EDGE ( 'NONE', *, *, #19004, .F. ) ;
#13760=EDGE_CURVE ( 'NONE', #15909, #16919, #10845, .T. ) ;
#13817=FACE_OUTER_BOUND ( 'NONE', #5420, .T. ) ;
#13830=CARTESIAN_POINT ( 'NONE',  ( -4.078421086530219064, -3.990950201428956845, -1.000000000000000000 ) ) ;
#13845=CIRCLE ( 'NONE', #4784, 4.799999999999999822 ) ;
#13871=DIRECTION ( 'NONE',  ( 1.000000000000000000, 0.000000000000000000, 0.000000000000000000 ) ) ;
#13879=ORIENTED_EDGE ( 'NONE', *, *, #18537, .F. ) ;
#13888=ORIENTED_EDGE ( 'NONE', *, *, #1800, .F. ) ;
#13918=AXIS2_PLACEMENT_3D ( 'NONE', #17369, #4688, #3124 ) ;
#13937=CARTESIAN_POINT ( 'NONE',  ( 2.595115354961440524, -7.673029147243177306, -1.000000000000000000 ) ) ;
#13947=AXIS2_PLACEMENT_3D ( 'NONE', #16365, #14774, #9087 ) ;
#13996=EDGE_LOOP ( 'NONE', ( #5328, #18030, #13709, #14884 ) ) ;
#14064=CARTESIAN_POINT ( 'NONE',  ( -0.5000000000000000000, -6.429618962271402616, -1.000000000000000000 ) ) ;
#14108=DIRECTION ( 'NONE',  ( 0.000000000000000000, 0.000000000000000000, 1.000000000000000000 ) ) ;
#14135=CARTESIAN_POINT ( 'NONE',  ( -0.5000000000000000000, -6.429618962271402616, 0.000000000000000000 ) ) ;
#14178=EDGE_CURVE ( 'NONE', #1126, #728, #7408, .T. ) ;
#14233=AXIS2_PLACEMENT_3D ( 'NONE', #8112, #10767, #17060 ) ;
#14282=DIRECTION ( 'NONE',  ( 0.000000000000000000, 0.000000000000000000, 1.000000000000000000 ) ) ;
#14303=CLOSED_SHELL ( 'NONE', ( #7737, #5378, #5560, #17096, #1175, #12764, #15381, #4416, #1741, #369, #7950, #5691, #19388, #3159, #19386, #13346, #17334, #15100, #2271, #10756, #11834, #3694 ) ) ;
#14351=CARTESIAN_POINT ( 'NONE',  ( 1.250000000000000000, -6.429618962271402616, -1.000000000000000000 ) ) ;
#14372=ORIENTED_EDGE ( 'NONE', *, *, #1256, .T. ) ;
#14377=VERTEX_POINT ( 'NONE', #3575 ) ;
#14384=DIRECTION ( 'NONE',  ( -0.000000000000000000, -0.000000000000000000, -1.000000000000000000 ) ) ;
#14401=DIRECTION ( 'NONE',  ( 0.000000000000000000, 0.000000000000000000, 1.000000000000000000 ) ) ;
#14402=APPLICATION_CONTEXT ( 'automotive_design' ) ;
#14409=CARTESIAN_POINT ( 'NONE',  ( 0.1481481481481481122, -4.797713218419819903, -1.000000000000000000 ) ) ;
#14427=VECTOR ( 'NONE', #5223, 1000.000000000000000 ) ;
#14453=DIRECTION ( 'NONE',  ( 0.000000000000000000, 0.000000000000000000, 1.000000000000000000 ) ) ;
#14462=DIRECTION ( 'NONE',  ( 1.000000000000000000, 0.000000000000000000, 0.000000000000000000 ) ) ;
#14493=CARTESIAN_POINT ( 'NONE',  ( -4.078421086530219064, -3.990950201428956845, -1.000000000000000000 ) ) ;
#14593=CARTESIAN_POINT ( 'NONE',  ( 4.799999999999999822, 0.000000000000000000, 0.000000000000000000 ) ) ;
#14626=EDGE_LOOP ( 'NONE', ( #8599, #2641, #8173, #12906 ) ) ;
#14641=VECTOR ( 'NONE', #11081, 1000.000000000000114 ) ;
#14662=VERTEX_POINT ( 'NONE', #1215 ) ;
#14678=CARTESIAN_POINT ( 'NONE',  ( -1.250000000000000000, -6.429618962271402616, 0.000000000000000000 ) ) ;
#14704=ORIENTED_EDGE ( 'NONE', *, *, #10466, .F. ) ;
#14736=AXIS2_PLACEMENT_3D ( 'NONE', #18955, #11274, #5112 ) ;
#14774=DIRECTION ( 'NONE',  ( 0.000000000000000000, 0.000000000000000000, 1.000000000000000000 ) ) ;
#14783=SHAPE_REPRESENTATION_RELATIONSHIP ( 'NONE' , 'NONE' ,  #11935, #15256 ) ;
#14787=ORIENTED_EDGE ( 'NONE', *, *, #17573, .F. ) ;
#14790=CIRCLE ( 'NONE', #7582, 4.799999999999999822 ) ;
#14794=UNCERTAINTY_MEASURE_WITH_UNIT (LENGTH_MEASURE( 1.000000000000000082E-05 ), #11448, 'distance_accuracy_value', 'NONE');
#14795=DIRECTION ( 'NONE',  ( 0.000000000000000000, 0.000000000000000000, 1.000000000000000000 ) ) ;
#14884=ORIENTED_EDGE ( 'NONE', *, *, #7166, .F. ) ;
#14908=CARTESIAN_POINT ( 'NONE',  ( -2.000000000000000000, -6.429618962271402616, -1.000000000000000000 ) ) ;
#14935=CARTESIAN_POINT ( 'NONE',  ( 4.078421086530217288, -3.990950201428958621, -1.000000000000000000 ) ) ;
#14962=AXIS2_PLACEMENT_3D ( 'NONE', #6967, #13046, #12755 ) ;
#14987=ORIENTED_EDGE ( 'NONE', *, *, #13760, .F. ) ;
#14989=VECTOR ( 'NONE', #10941, 999.9999999999998863 ) ;
#15074=CARTESIAN_POINT ( 'NONE',  ( 2.354826896168714434, -6.962563485461402024, 0.000000000000000000 ) ) ;
#15100=ADVANCED_FACE ( 'NONE', ( #6159 ), #10559, .T. ) ;
#15130=CARTESIAN_POINT ( 'NONE',  ( -0.1481481481481481122, -4.797713218419819903, 0.000000000000000000 ) ) ;
#15132=LINE ( 'NONE', #139, #6462 ) ;
#15170=ORIENTED_EDGE ( 'NONE', *, *, #18537, .T. ) ;
#15205=EDGE_CURVE ( 'NONE', #11016, #11915, #6350, .T. ) ;
#15213=DIRECTION ( 'NONE',  ( 1.000000000000000000, 0.000000000000000000, 0.000000000000000000 ) ) ;
#15256=ADVANCED_BREP_SHAPE_REPRESENTATION ( '', ( #8790, #10359 ), #11203 ) ;
#15351=AXIS2_PLACEMENT_3D ( 'NONE', #1645, #161, #13497 ) ;
#15381=ADVANCED_FACE ( 'NONE', ( #15660 ), #11232, .F. ) ;
#15501=AXIS2_PLACEMENT_3D ( 'NONE', #15074, #12024, #18025 ) ;
#15532=EDGE_LOOP ( 'NONE', ( #14987, #13176, #2146, #12999 ) ) ;
#15567=ORIENTED_EDGE ( 'NONE', *, *, #525, .F. ) ;
#15596=DIRECTION ( 'NONE',  ( 1.000000000000000000, 0.000000000000000000, 0.000000000000000000 ) ) ;
#15660=FACE_OUTER_BOUND ( 'NONE', #2434, .T. ) ;
#15664=AXIS2_PLACEMENT_3D ( 'NONE', #8788, #17727, #5754 ) ;
#15700=CARTESIAN_POINT ( 'NONE',  ( 0.000000000000000000, 0.000000000000000000, 0.000000000000000000 ) ) ;
#15709=CIRCLE ( 'NONE', #7256, 0.7500000000000000000 ) ;
#15765=ORIENTED_EDGE ( 'NONE', *, *, #13610, .T. ) ;
#15771=VERTEX_POINT ( 'NONE', #6995 ) ;
#15781=DIRECTION ( 'NONE',  ( 0.000000000000000000, 0.000000000000000000, 1.000000000000000000 ) ) ;
#15849=EDGE_LOOP ( 'NONE', ( #10153, #3604, #2965, #2704, #13557, #2158, #5540, #1951, #11994, #11316, #17792, #17717, #1071, #307, #16733, #3618 ) ) ;
#15875=LINE ( 'NONE', #2659, #2789 ) ;
#15909=VERTEX_POINT ( 'NONE', #12687 ) ;
#15931=DIRECTION ( 'NONE',  ( 0.000000000000000000, 0.000000000000000000, 1.000000000000000000 ) ) ;
#16001=FACE_OUTER_BOUND ( 'NONE', #16755, .T. ) ;
#16002=EDGE_CURVE ( 'NONE', #8267, #5177, #16586, .T. ) ;
#16019=CARTESIAN_POINT ( 'NONE',  ( 0.5000000000000000000, -6.429618962271402616, 0.000000000000000000 ) ) ;
#16055=EDGE_CURVE ( 'NONE', #4604, #16860, #2795, .T. ) ;
#16085=CARTESIAN_POINT ( 'NONE',  ( 4.799999999999999822, 0.000000000000000000, -1.000000000000000000 ) ) ;
#16128=FACE_BOUND ( 'NONE', #5335, .T. ) ;
#16136=AXIS2_PLACEMENT_3D ( 'NONE', #8914, #7349, #3048 ) ;
#16163=CARTESIAN_POINT ( 'NONE',  ( 6.080745460913608902, 0.5192545390863916310, -1.000000000000000000 ) ) ;
#16172=DIRECTION ( 'NONE',  ( 0.000000000000000000, 0.000000000000000000, 1.000000000000000000 ) ) ;
#16179=DIRECTION ( 'NONE',  ( 0.000000000000000000, 0.000000000000000000, 1.000000000000000000 ) ) ;
#16180=UNCERTAINTY_MEASURE_WITH_UNIT (LENGTH_MEASURE( 1.000000000000000082E-05 ), #2564, 'distance_accuracy_value', 'NONE');
#16191=DIRECTION ( 'NONE',  ( 1.000000000000000000, 0.000000000000000000, 0.000000000000000000 ) ) ;
#16199=LINE ( 'NONE', #17773, #4631 ) ;
#16223=ORIENTED_EDGE ( 'NONE', *, *, #7372, .F. ) ;
#16224=CARTESIAN_POINT ( 'NONE',  ( 1.250000000000000000, -6.429618962271402616, 0.000000000000000000 ) ) ;
#16245=VECTOR ( 'NONE', #16172, 1000.000000000000000 ) ;
#16255=DIRECTION ( 'NONE',  ( 0.000000000000000000, 0.000000000000000000, 1.000000000000000000 ) ) ;
#16359=EDGE_CURVE ( 'NONE', #983, #15909, #3651, .T. ) ;
#16365=CARTESIAN_POINT ( 'NONE',  ( 0.000000000000000000, 0.000000000000000000, -1.000000000000000000 ) ) ;
#16394=EDGE_LOOP ( 'NONE', ( #6977, #11500, #18882, #12717 ) ) ;
#16426=DIRECTION ( 'NONE',  ( 0.03086419753086420623, 0.9995235871707959241, -0.000000000000000000 ) ) ;
#16445=CARTESIAN_POINT ( 'NONE',  ( -0.1481481481481481122, -4.797713218419819903, -1.000000000000000000 ) ) ;
#16451=CARTESIAN_POINT ( 'NONE',  ( -6.080745460913608902, 0.5192545390863924082, -1.000000000000000000 ) ) ;
#16459=DIRECTION ( 'NONE',  ( 0.000000000000000000, 0.000000000000000000, 1.000000000000000000 ) ) ;
#16474=EDGE_LOOP ( 'NONE', ( #16775, #6852 ) ) ;
#16512=AXIS2_PLACEMENT_3D ( 'NONE', #11604, #10131, #8663 ) ;
#16533=VERTEX_POINT ( 'NONE', #4330 ) ;
#16586=CIRCLE ( 'NONE', #11869, 0.7500000000000000000 ) ;
#16593=EDGE_CURVE ( 'NONE', #983, #3316, #9216, .T. ) ;
#16632=AXIS2_PLACEMENT_3D ( 'NONE', #5567, #6943, #9783 ) ;
#16633=AXIS2_PLACEMENT_3D ( 'NONE', #5523, #15931, #12889 ) ;
#16675=DIRECTION ( 'NONE',  ( 0.1305261922200524338, -0.9914448613738102711, 0.000000000000000000 ) ) ;
#16733=ORIENTED_EDGE ( 'NONE', *, *, #2475, .F. ) ;
#16755=EDGE_LOOP ( 'NONE', ( #19378, #17729, #4190, #9971 ) ) ;
#16775=ORIENTED_EDGE ( 'NONE', *, *, #12082, .T. ) ;
#16860=VERTEX_POINT ( 'NONE', #9496 ) ;
#16872=ORIENTED_EDGE ( 'NONE', *, *, #1106, .F. ) ;
#16878=ORIENTED_EDGE ( 'NONE', *, *, #18301, .T. ) ;
#16896=FACE_OUTER_BOUND ( 'NONE', #5448, .T. ) ;
#16919=VERTEX_POINT ( 'NONE', #17270 ) ;
#16938=CIRCLE ( 'NONE', #8775, 4.799999999999999822 ) ;
#16940=CARTESIAN_POINT ( 'NONE',  ( -2.354826896168714434, -6.962563485461402024, 0.000000000000000000 ) ) ;
#16950=EDGE_CURVE ( 'NONE', #1126, #9852, #5326, .T. ) ;
#16961=ORIENTED_EDGE ( 'NONE', *, *, #6305, .T. ) ;
#16962=EDGE_CURVE ( 'NONE', #10892, #8318, #8134, .T. ) ;
#16974=CIRCLE ( 'NONE', #1632, 0.7499999999999997780 ) ;
#17039=CARTESIAN_POINT ( 'NONE',  ( -1.250000000000000000, -6.429618962271402616, -1.000000000000000000 ) ) ;
#17060=DIRECTION ( 'NONE',  ( 1.000000000000000000, 0.000000000000000000, 0.000000000000000000 ) ) ;
#17096=ADVANCED_FACE ( 'NONE', ( #9499 ), #8131, .T. ) ;
#17114=EDGE_CURVE ( 'NONE', #8527, #5177, #18741, .T. ) ;
#17133=CARTESIAN_POINT ( 'NONE',  ( 2.000000000000000000, -6.429618962271402616, 0.000000000000000000 ) ) ;
#17158=ORIENTED_EDGE ( 'NONE', *, *, #10711, .F. ) ;
#17179=CYLINDRICAL_SURFACE ( 'NONE', #18426, 4.799999999999999822 ) ;
#17198=LINE ( 'NONE', #7965, #12774 ) ;
#17234=ORIENTED_EDGE ( 'NONE', *, *, #5617, .T. ) ;
#17245=EDGE_LOOP ( 'NONE', ( #17637, #10344, #1348, #1319 ) ) ;
#17256=FACE_BOUND ( 'NONE', #16474, .T. ) ;
#17270=CARTESIAN_POINT ( 'NONE',  ( -3.098410542199071749, -7.060458129626440815, 0.000000000000000000 ) ) ;
#17287=AXIS2_PLACEMENT_3D ( 'NONE', #11078, #18661, #6473 ) ;
#17303=DIRECTION ( 'NONE',  ( 0.000000000000000000, 0.000000000000000000, 1.000000000000000000 ) ) ;
#17309=ORIENTED_EDGE ( 'NONE', *, *, #2388, .F. ) ;
#17326=EDGE_CURVE ( 'NONE', #2828, #17434, #1082, .T. ) ;
#17332=ORIENTED_EDGE ( 'NONE', *, *, #4748, .F. ) ;
#17334=ADVANCED_FACE ( 'NONE', ( #18943 ), #8819, .T. ) ;
#17346=CARTESIAN_POINT ( 'NONE',  ( 0.1481481481481481122, -4.797713218419819903, -1.000000000000000000 ) ) ;
#17369=CARTESIAN_POINT ( 'NONE',  ( 5.686050877451574337, -5.768780236673276995, -1.000000000000000000 ) ) ;
#17379=FACE_OUTER_BOUND ( 'NONE', #12855, .T. ) ;
#17418=CARTESIAN_POINT ( 'NONE',  ( 2.595115354961440524, -7.673029147243177306, 0.000000000000000000 ) ) ;
#17429=ORIENTED_EDGE ( 'NONE', *, *, #15205, .T. ) ;
#17434=VERTEX_POINT ( 'NONE', #14593 ) ;
#17472=DIRECTION ( 'NONE',  ( 0.000000000000000000, 0.000000000000000000, 1.000000000000000000 ) ) ;
#17512=CARTESIAN_POINT ( 'NONE',  ( -6.080745460913608902, 0.5192545390863924082, 0.000000000000000000 ) ) ;
#17517=CARTESIAN_POINT ( 'NONE',  ( 0.000000000000000000, 0.000000000000000000, 0.000000000000000000 ) ) ;
#17566=CARTESIAN_POINT ( 'NONE',  ( 0.000000000000000000, 0.000000000000000000, -1.000000000000000000 ) ) ;
#17573=EDGE_CURVE ( 'NONE', #16533, #15771, #12241, .T. ) ;
#17576=DIRECTION ( 'NONE',  ( 1.000000000000000000, 0.000000000000000000, 0.000000000000000000 ) ) ;
#17609=CARTESIAN_POINT ( 'NONE',  ( -1.250000000000000000, -6.429618962271402616, 0.000000000000000000 ) ) ;
#17629=AXIS2_PLACEMENT_3D ( 'NONE', #19094, #8484, #14462 ) ;
#17637=ORIENTED_EDGE ( 'NONE', *, *, #8435, .F. ) ;
#17652=LINE ( 'NONE', #4203, #16245 ) ;
#17653=CARTESIAN_POINT ( 'NONE',  ( 1.250000000000000000, -6.429618962271402616, -1.000000000000000000 ) ) ;
#17663=FACE_OUTER_BOUND ( 'NONE', #10415, .T. ) ;
#17683=CARTESIAN_POINT ( 'NONE',  ( -1.250000000000000000, -6.429618962271402616, -1.000000000000000000 ) ) ;
#17694=ORIENTED_EDGE ( 'NONE', *, *, #16002, .T. ) ;
#17717=ORIENTED_EDGE ( 'NONE', *, *, #16950, .F. ) ;
#17727=DIRECTION ( 'NONE',  ( 0.000000000000000000, 0.000000000000000000, 1.000000000000000000 ) ) ;
#17729=ORIENTED_EDGE ( 'NONE', *, *, #13610, .F. ) ;
#17773=CARTESIAN_POINT ( 'NONE',  ( 3.309651814758565180, -5.455921364805393026, 0.000000000000000000 ) ) ;
#17791=STYLED_ITEM('',(#19468),#8790);
#17792=ORIENTED_EDGE ( 'NONE', *, *, #3531, .F. ) ;
#17793=EDGE_CURVE ( 'NONE', #8318, #2946, #4696, .T. ) ;
#17803=CARTESIAN_POINT ( 'NONE',  ( 0.000000000000000000, 0.000000000000000000, -1.000000000000000000 ) ) ;
#17804=AXIS2_PLACEMENT_3D ( 'NONE', #13724, #303, #12253 ) ;
#17824=CARTESIAN_POINT ( 'NONE',  ( 0.000000000000000000, 0.000000000000000000, -1.000000000000000000 ) ) ;
#17826=VERTEX_POINT ( 'NONE', #8049 ) ;
#17872=EDGE_LOOP ( 'NONE', ( #5621, #16223, #5426, #5157 ) ) ;
#17903=CARTESIAN_POINT ( 'NONE',  ( -0.1481481481481481122, -4.797713218419819903, -1.000000000000000000 ) ) ;
#17922=LINE ( 'NONE', #16445, #18825 ) ;
#17928=ORIENTED_EDGE ( 'NONE', *, *, #12398, .T. ) ;
#17935=CARTESIAN_POINT ( 'NONE',  ( -2.000000000000000000, -6.429618962271402616, 0.000000000000000000 ) ) ;
#18011=DIRECTION ( 'NONE',  ( 0.000000000000000000, 0.000000000000000000, 1.000000000000000000 ) ) ;
#18016=VECTOR ( 'NONE', #14282, 1000.000000000000000 ) ;
#18025=DIRECTION ( 'NONE',  ( -1.000000000000000000, 0.000000000000000000, 0.000000000000000000 ) ) ;
#18026=CARTESIAN_POINT ( 'NONE',  ( 4.078421086530217288, -3.990950201428958621, 0.000000000000000000 ) ) ;
#18030=ORIENTED_EDGE ( 'NONE', *, *, #4748, .T. ) ;
#18076=VECTOR ( 'NONE', #16426, 1000.000000000000114 ) ;
#18093=DIRECTION ( 'NONE',  ( 0.000000000000000000, 0.000000000000000000, 1.000000000000000000 ) ) ;
#18114=AXIS2_PLACEMENT_3D ( 'NONE', #6689, #12672, #3562 ) ;
#18139=CARTESIAN_POINT ( 'NONE',  ( 0.1481481481481481122, -4.797713218419819903, -1.000000000000000000 ) ) ;
#18187=EDGE_CURVE ( 'NONE', #8385, #2130, #10310, .T. ) ;
#18188=VERTEX_POINT ( 'NONE', #17133 ) ;
#18230=CARTESIAN_POINT ( 'NONE',  ( 0.1481481481481481122, -4.797713218419819903, 0.000000000000000000 ) ) ;
#18232=DIRECTION ( 'NONE',  ( 1.000000000000000000, 0.000000000000000000, 0.000000000000000000 ) ) ;
#18242=ORIENTED_EDGE ( 'NONE', *, *, #773, .T. ) ;
#18247=CARTESIAN_POINT ( 'NONE',  ( -2.595115354961444076, -7.673029147243174641, -1.000000000000000000 ) ) ;
#18275=CARTESIAN_POINT ( 'NONE',  ( 0.1481481481481481122, -4.797713218419819903, -1.000000000000000000 ) ) ;
#18286=ORIENTED_EDGE ( 'NONE', *, *, #10579, .T. ) ;
#18301=EDGE_CURVE ( 'NONE', #8527, #13173, #13134, .T. ) ;
#18326=ORIENTED_EDGE ( 'NONE', *, *, #1106, .T. ) ;
#18333=EDGE_LOOP ( 'NONE', ( #1755, #15170, #3487, #3250 ) ) ;
#18343=AXIS2_PLACEMENT_3D ( 'NONE', #5290, #14401, #13035 ) ;
#18405=DIRECTION ( 'NONE',  ( 1.000000000000000000, 0.000000000000000000, 0.000000000000000000 ) ) ;
#18426=AXIS2_PLACEMENT_3D ( 'NONE', #3459, #7765, #11173 ) ;
#18512=CIRCLE ( 'NONE', #16632, 6.080745460913608902 ) ;
#18537=EDGE_CURVE ( 'NONE', #8815, #8974, #11708, .T. ) ;
#18539=PRODUCT_DEFINITION_CONTEXT ( 'detailed design', #14402, 'design' ) ;
#18661=DIRECTION ( 'NONE',  ( 0.000000000000000000, 0.000000000000000000, 1.000000000000000000 ) ) ;
#18691=LINE ( 'NONE', #12689, #5659 ) ;
#18717=EDGE_LOOP ( 'NONE', ( #10398, #2571, #11234, #5357 ) ) ;
#18741=LINE ( 'NONE', #6566, #12856 ) ;
#18743=CYLINDRICAL_SURFACE ( 'NONE', #18343, 0.7499999999999997780 ) ;
#18767=FACE_OUTER_BOUND ( 'NONE', #8999, .T. ) ;
#18772=CARTESIAN_POINT ( 'NONE',  ( -3.098410542199071749, -7.060458129626440815, -1.000000000000000000 ) ) ;
#18825=VECTOR ( 'NONE', #8880, 1000.000000000000000 ) ;
#18882=ORIENTED_EDGE ( 'NONE', *, *, #11926, .T. ) ;
#18912=ORIENTED_EDGE ( 'NONE', *, *, #17114, .T. ) ;
#18943=FACE_OUTER_BOUND ( 'NONE', #18717, .T. ) ;
#18955=CARTESIAN_POINT ( 'NONE',  ( 0.000000000000000000, 0.5192545390863916310, -1.000000000000000000 ) ) ;
#18969=CIRCLE ( 'NONE', #15501, 0.7499999999999997780 ) ;
#18977=ORIENTED_EDGE ( 'NONE', *, *, #8435, .T. ) ;
#19004=EDGE_CURVE ( 'NONE', #11693, #11530, #12850, .T. ) ;
#19023=DIRECTION ( 'NONE',  ( 1.000000000000000000, 0.000000000000000000, 0.000000000000000000 ) ) ;
#19032=CIRCLE ( 'NONE', #9907, 0.7500000000000000000 ) ;
#19094=CARTESIAN_POINT ( 'NONE',  ( 5.686050877451574337, -5.768780236673276995, 0.000000000000000000 ) ) ;
#19104=VECTOR ( 'NONE', #18011, 1000.000000000000000 ) ;
#19115=ORIENTED_EDGE ( 'NONE', *, *, #18301, .F. ) ;
#19131=PRESENTATION_STYLE_ASSIGNMENT (( #4301 ) ) ;
#19142=ORIENTED_EDGE ( 'NONE', *, *, #18187, .F. ) ;
#19183=VECTOR ( 'NONE', #11368, 1000.000000000000000 ) ;
#19209=CARTESIAN_POINT ( 'NONE',  ( 2.595115354961440524, -7.673029147243177306, -1.000000000000000000 ) ) ;
#19282=( GEOMETRIC_REPRESENTATION_CONTEXT ( 3 ) GLOBAL_UNCERTAINTY_ASSIGNED_CONTEXT ( ( #6544 ) ) GLOBAL_UNIT_ASSIGNED_CONTEXT ( ( #7590, #1811, #11897 ) ) REPRESENTATION_CONTEXT ( 'NONE', 'WORKASPACE' ) );
#19288=DIRECTION ( 'NONE',  ( 1.000000000000000000, 0.000000000000000000, 0.000000000000000000 ) ) ;
#19310=DIRECTION ( 'NONE',  ( 0.000000000000000000, 0.000000000000000000, 1.000000000000000000 ) ) ;
#19335=CARTESIAN_POINT ( 'NONE',  ( 3.098410542199072637, -7.060458129626440815, -1.000000000000000000 ) ) ;
#19378=ORIENTED_EDGE ( 'NONE', *, *, #12398, .F. ) ;
#19386=ADVANCED_FACE ( 'NONE', ( #16001 ), #6968, .T. ) ;
#19388=ADVANCED_FACE ( 'NONE', ( #17379 ), #6578, .T. ) ;
#19415=( GEOMETRIC_REPRESENTATION_CONTEXT ( 3 ) GLOBAL_UNCERTAINTY_ASSIGNED_CONTEXT ( ( #16180 ) ) GLOBAL_UNIT_ASSIGNED_CONTEXT ( ( #2564, #13024, #10267 ) ) REPRESENTATION_CONTEXT ( 'NONE', 'WORKASPACE' ) );
#19462=COLOUR_RGB('Grey',0.48,0.52,0.57);
#19463=FILL_AREA_STYLE_COLOUR('',#19462);
#19464=FILL_AREA_STYLE('',(#19463));
#19465=SURFACE_STYLE_FILL_AREA(#19464);
#19466=SURFACE_SIDE_STYLE('',(#19465));
#19467=SURFACE_STYLE_USAGE(.BOTH.,#19466);
#19468=PRESENTATION_STYLE_ASSIGNMENT((#19467));
ENDSEC;
END-ISO-10303-21;
